ISO-10303-21;
HEADER;
/* Generated by software containing ST-Developer
 * from STEP Tools, Inc. (www.steptools.com) 
 */
/* OPTION: using custom renumber hook */

FILE_DESCRIPTION(
/* description */ ('STEP AP242 Edition 2', 'CAx-IF Rec.Pracs.---Representation and Presentation of Product Manufa
cturing Information (PMI)---4.0---2014-10-13', 'CAx-IF Rec.Pracs.---3D Tessellated Geometry---0.4---2014-09-14', '2;1', 'CAx-IF Rec.Pracs.---User Defined Attributes---1.5---2016-08-15'),
/* implementation_level */ '2;1');

FILE_NAME(
/* name */ 'Part 1__PD10223.step',
/* time_stamp */ '2026-10-09T13:59:33Z',
/* author */ (''),
/* organization */ (''),
/* preprocessor_version */ 'ST-DEVELOPER v20',
/* originating_system */ 'ONSHAPE BY PTC INC, 1.221',
/* authorisation */ '  ');

FILE_SCHEMA (('AP242_MANAGED_MODEL_BASED_3D_ENGINEERING_MIM_LF { 1 0 10303 442 3 1 4 }'));
ENDSEC;

DATA;
#13=CONICAL_SURFACE('',#6425,0.0619081467766146,1.18042781059053);
#14=CONICAL_SURFACE('',#6427,0.0645,1.46120958979089);
#25=TOROIDAL_SURFACE('',#6439,0.0635,0.001);
#26=TOROIDAL_SURFACE('',#6441,0.0635,0.001);
#27=TOROIDAL_SURFACE('',#6442,0.0639081467766146,0.001);
#28=TOROIDAL_SURFACE('',#6444,0.0635863977385909,0.001);
#29=TOROIDAL_SURFACE('',#6446,0.0635,0.001);
#30=TOROIDAL_SURFACE('',#6448,0.0629081467766146,0.001);
#31=TOROIDAL_SURFACE('',#6449,0.0644389218390369,0.001);
#682=SHAPE_REPRESENTATION_RELATIONSHIP('','',#5701,#696);
#696=ADVANCED_BREP_SHAPE_REPRESENTATION('',(#5669),#10155);
#773=PLANE('',#6421);
#774=PLANE('',#6432);
#775=PLANE('',#6438);
#2196=ORIENTED_EDGE('',*,*,#3035,.F.);
#2197=ORIENTED_EDGE('',*,*,#3036,.T.);
#2198=ORIENTED_EDGE('',*,*,#3036,.F.);
#2199=ORIENTED_EDGE('',*,*,#3037,.T.);
#2200=ORIENTED_EDGE('',*,*,#3037,.F.);
#2201=ORIENTED_EDGE('',*,*,#3038,.T.);
#2202=ORIENTED_EDGE('',*,*,#3038,.F.);
#2203=ORIENTED_EDGE('',*,*,#3039,.T.);
#2204=ORIENTED_EDGE('',*,*,#3040,.T.);
#2205=ORIENTED_EDGE('',*,*,#3039,.F.);
#2206=ORIENTED_EDGE('',*,*,#3041,.T.);
#2207=ORIENTED_EDGE('',*,*,#3042,.T.);
#2208=ORIENTED_EDGE('',*,*,#3043,.T.);
#2209=ORIENTED_EDGE('',*,*,#3044,.T.);
#2210=ORIENTED_EDGE('',*,*,#3045,.T.);
#2211=ORIENTED_EDGE('',*,*,#3046,.T.);
#2212=ORIENTED_EDGE('',*,*,#3046,.F.);
#2213=ORIENTED_EDGE('',*,*,#3035,.T.);
#2214=ORIENTED_EDGE('',*,*,#3047,.T.);
#2215=ORIENTED_EDGE('',*,*,#3041,.F.);
#2216=ORIENTED_EDGE('',*,*,#3042,.F.);
#2217=ORIENTED_EDGE('',*,*,#3040,.F.);
#2218=ORIENTED_EDGE('',*,*,#3048,.F.);
#2219=ORIENTED_EDGE('',*,*,#3047,.F.);
#2220=ORIENTED_EDGE('',*,*,#3049,.T.);
#2221=ORIENTED_EDGE('',*,*,#3048,.T.);
#2222=ORIENTED_EDGE('',*,*,#3050,.F.);
#2223=ORIENTED_EDGE('',*,*,#3049,.F.);
#2224=ORIENTED_EDGE('',*,*,#3045,.F.);
#2225=ORIENTED_EDGE('',*,*,#3043,.F.);
#2226=ORIENTED_EDGE('',*,*,#3044,.F.);
#2227=ORIENTED_EDGE('',*,*,#3050,.T.);
#3035=EDGE_CURVE('',#3593,#3593,#4066,.T.);
#3036=EDGE_CURVE('',#3594,#3594,#4067,.T.);
#3037=EDGE_CURVE('',#3595,#3595,#4068,.T.);
#3038=EDGE_CURVE('',#3596,#3596,#4069,.T.);
#3039=EDGE_CURVE('',#3597,#3597,#4070,.T.);
#3040=EDGE_CURVE('',#3598,#3598,#4071,.T.);
#3041=EDGE_CURVE('',#3599,#3599,#4072,.T.);
#3042=EDGE_CURVE('',#3600,#3600,#4073,.T.);
#3043=EDGE_CURVE('',#3601,#3601,#4074,.T.);
#3044=EDGE_CURVE('',#3602,#3602,#4075,.F.);
#3045=EDGE_CURVE('',#3603,#3603,#4076,.F.);
#3046=EDGE_CURVE('',#3604,#3604,#4077,.T.);
#3047=EDGE_CURVE('',#3605,#3605,#4078,.T.);
#3048=EDGE_CURVE('',#3606,#3606,#4079,.F.);
#3049=EDGE_CURVE('',#3607,#3607,#4080,.T.);
#3050=EDGE_CURVE('',#3608,#3608,#4081,.T.);
#3593=VERTEX_POINT('',#9942);
#3594=VERTEX_POINT('',#9944);
#3595=VERTEX_POINT('',#9947);
#3596=VERTEX_POINT('',#9950);
#3597=VERTEX_POINT('',#9953);
#3598=VERTEX_POINT('',#9956);
#3599=VERTEX_POINT('',#9959);
#3600=VERTEX_POINT('',#9961);
#3601=VERTEX_POINT('',#9964);
#3602=VERTEX_POINT('',#9966);
#3603=VERTEX_POINT('',#9969);
#3604=VERTEX_POINT('',#9971);
#3605=VERTEX_POINT('',#9975);
#3606=VERTEX_POINT('',#9979);
#3607=VERTEX_POINT('',#9982);
#3608=VERTEX_POINT('',#9985);
#4066=CIRCLE('',#6419,0.0635);
#4067=CIRCLE('',#6420,0.0635);
#4068=CIRCLE('',#6422,0.06);
#4069=CIRCLE('',#6424,0.06);
#4070=CIRCLE('',#6426,0.0619081467766146);
#4071=CIRCLE('',#6428,0.0636093675261996);
#4072=CIRCLE('',#6430,0.0645);
#4073=CIRCLE('',#6431,0.0645);
#4074=CIRCLE('',#6433,0.0629081467766146);
#4075=CIRCLE('',#6434,0.0644389218390369);
#4076=CIRCLE('',#6436,0.0619081467766146);
#4077=CIRCLE('',#6437,0.0619081467766146);
#4078=CIRCLE('',#6440,0.0637040733883139);
#4079=CIRCLE('',#6443,0.0629081467766146);
#4080=CIRCLE('',#6445,0.0635431988692856);
#4081=CIRCLE('',#6447,0.0645);
#4488=EDGE_LOOP('',(#2196));
#4489=EDGE_LOOP('',(#2197));
#4490=EDGE_LOOP('',(#2198));
#4491=EDGE_LOOP('',(#2199));
#4492=EDGE_LOOP('',(#2200));
#4493=EDGE_LOOP('',(#2201));
#4494=EDGE_LOOP('',(#2202));
#4495=EDGE_LOOP('',(#2203));
#4496=EDGE_LOOP('',(#2204));
#4497=EDGE_LOOP('',(#2205));
#4498=EDGE_LOOP('',(#2206));
#4499=EDGE_LOOP('',(#2207));
#4500=EDGE_LOOP('',(#2208));
#4501=EDGE_LOOP('',(#2209));
#4502=EDGE_LOOP('',(#2210));
#4503=EDGE_LOOP('',(#2211));
#4504=EDGE_LOOP('',(#2212));
#4505=EDGE_LOOP('',(#2213));
#4506=EDGE_LOOP('',(#2214));
#4507=EDGE_LOOP('',(#2215));
#4508=EDGE_LOOP('',(#2216));
#4509=EDGE_LOOP('',(#2217));
#4510=EDGE_LOOP('',(#2218));
#4511=EDGE_LOOP('',(#2219));
#4512=EDGE_LOOP('',(#2220));
#4513=EDGE_LOOP('',(#2221));
#4514=EDGE_LOOP('',(#2222));
#4515=EDGE_LOOP('',(#2223));
#4516=EDGE_LOOP('',(#2224));
#4517=EDGE_LOOP('',(#2225));
#4518=EDGE_LOOP('',(#2226));
#4519=EDGE_LOOP('',(#2227));
#4936=FACE_BOUND('',#4488,.T.);
#4937=FACE_BOUND('',#4489,.T.);
#4938=FACE_BOUND('',#4490,.T.);
#4939=FACE_BOUND('',#4491,.T.);
#4940=FACE_BOUND('',#4492,.T.);
#4941=FACE_BOUND('',#4493,.T.);
#4942=FACE_BOUND('',#4494,.T.);
#4943=FACE_BOUND('',#4495,.T.);
#4944=FACE_BOUND('',#4496,.T.);
#4945=FACE_BOUND('',#4497,.T.);
#4946=FACE_BOUND('',#4498,.T.);
#4947=FACE_BOUND('',#4499,.T.);
#4948=FACE_BOUND('',#4500,.T.);
#4949=FACE_BOUND('',#4501,.T.);
#4950=FACE_BOUND('',#4502,.T.);
#4951=FACE_BOUND('',#4503,.T.);
#4952=FACE_BOUND('',#4504,.T.);
#4953=FACE_BOUND('',#4505,.T.);
#4954=FACE_BOUND('',#4506,.T.);
#4955=FACE_BOUND('',#4507,.T.);
#4956=FACE_BOUND('',#4508,.T.);
#4957=FACE_BOUND('',#4509,.T.);
#4958=FACE_BOUND('',#4510,.T.);
#4959=FACE_BOUND('',#4511,.T.);
#4960=FACE_BOUND('',#4512,.T.);
#4961=FACE_BOUND('',#4513,.T.);
#4962=FACE_BOUND('',#4514,.T.);
#4963=FACE_BOUND('',#4515,.T.);
#4964=FACE_BOUND('',#4516,.T.);
#4965=FACE_BOUND('',#4517,.T.);
#4966=FACE_BOUND('',#4518,.T.);
#4967=FACE_BOUND('',#4519,.T.);
#5201=CYLINDRICAL_SURFACE('',#6418,0.0635);
#5202=CYLINDRICAL_SURFACE('',#6423,0.06);
#5203=CYLINDRICAL_SURFACE('',#6429,0.0645);
#5204=CYLINDRICAL_SURFACE('',#6435,0.0619081467766146);
#5496=ADVANCED_FACE('',(#4936,#4937),#5201,.F.);
#5497=ADVANCED_FACE('',(#4938,#4939),#773,.F.);
#5498=ADVANCED_FACE('',(#4940,#4941),#5202,.F.);
#5499=ADVANCED_FACE('',(#4942,#4943),#13,.F.);
#5500=ADVANCED_FACE('',(#4944,#4945),#14,.T.);
#5501=ADVANCED_FACE('',(#4946,#4947),#5203,.T.);
#5502=ADVANCED_FACE('',(#4948,#4949),#774,.F.);
#5503=ADVANCED_FACE('',(#4950,#4951),#5204,.F.);
#5504=ADVANCED_FACE('',(#4952,#4953),#775,.F.);
#5505=ADVANCED_FACE('',(#4954,#4955),#25,.T.);
#5506=ADVANCED_FACE('',(#4956,#4957),#26,.T.);
#5507=ADVANCED_FACE('',(#4958,#4959),#27,.F.);
#5508=ADVANCED_FACE('',(#4960,#4961),#28,.F.);
#5509=ADVANCED_FACE('',(#4962,#4963),#29,.T.);
#5510=ADVANCED_FACE('',(#4964,#4965),#30,.T.);
#5511=ADVANCED_FACE('',(#4966,#4967),#31,.T.);
#5550=CLOSED_SHELL('',(#5496,#5497,#5498,#5499,#5500,#5501,#5502,#5503,
#5504,#5505,#5506,#5507,#5508,#5509,#5510,#5511));
#5564=STYLED_ITEM('',(#5578),#5669);
#5578=PRESENTATION_STYLE_ASSIGNMENT((#5592));
#5592=SURFACE_STYLE_USAGE(.BOTH.,#5606);
#5606=SURFACE_SIDE_STYLE('',(#5620));
#5620=SURFACE_STYLE_FILL_AREA(#5634);
#5634=FILL_AREA_STYLE('',(#5648));
#5648=FILL_AREA_STYLE_COLOUR('',#5651);
#5651=COLOUR_RGB('', 0.66274510, 0.83137255, 0.94901961);
#5669=MANIFOLD_SOLID_BREP('Part 1',#5550);
#5685=SHAPE_DEFINITION_REPRESENTATION(#10204,#5701);
#5701=SHAPE_REPRESENTATION('Part 1',(#5704),#10155);
#5704=AXIS2_PLACEMENT_3D('',#8391,#6505,#6506);
#6418=AXIS2_PLACEMENT_3D('',#9940,#8192,#8193);
#6419=AXIS2_PLACEMENT_3D('',#9941,#8194,#8195);
#6420=AXIS2_PLACEMENT_3D('',#9943,#8196,#8197);
#6421=AXIS2_PLACEMENT_3D('',#9945,#8198,#8199);
#6422=AXIS2_PLACEMENT_3D('',#9946,#8200,#8201);
#6423=AXIS2_PLACEMENT_3D('',#9948,#8202,#8203);
#6424=AXIS2_PLACEMENT_3D('',#9949,#8204,#8205);
#6425=AXIS2_PLACEMENT_3D('',#9951,#8206,#8207);
#6426=AXIS2_PLACEMENT_3D('',#9952,#8208,#8209);
#6427=AXIS2_PLACEMENT_3D('',#9954,#8210,#8211);
#6428=AXIS2_PLACEMENT_3D('',#9955,#8212,#8213);
#6429=AXIS2_PLACEMENT_3D('',#9957,#8214,#8215);
#6430=AXIS2_PLACEMENT_3D('',#9958,#8216,#8217);
#6431=AXIS2_PLACEMENT_3D('',#9960,#8218,#8219);
#6432=AXIS2_PLACEMENT_3D('',#9962,#8220,#8221);
#6433=AXIS2_PLACEMENT_3D('',#9963,#8222,#8223);
#6434=AXIS2_PLACEMENT_3D('',#9965,#8224,#8225);
#6435=AXIS2_PLACEMENT_3D('',#9967,#8226,#8227);
#6436=AXIS2_PLACEMENT_3D('',#9968,#8228,#8229);
#6437=AXIS2_PLACEMENT_3D('',#9970,#8230,#8231);
#6438=AXIS2_PLACEMENT_3D('',#9972,#8232,#8233);
#6439=AXIS2_PLACEMENT_3D('',#9973,#8234,#8235);
#6440=AXIS2_PLACEMENT_3D('',#9974,#8236,#8237);
#6441=AXIS2_PLACEMENT_3D('',#9976,#8238,#8239);
#6442=AXIS2_PLACEMENT_3D('',#9977,#8240,#8241);
#6443=AXIS2_PLACEMENT_3D('',#9978,#8242,#8243);
#6444=AXIS2_PLACEMENT_3D('',#9980,#8244,#8245);
#6445=AXIS2_PLACEMENT_3D('',#9981,#8246,#8247);
#6446=AXIS2_PLACEMENT_3D('',#9983,#8248,#8249);
#6447=AXIS2_PLACEMENT_3D('',#9984,#8250,#8251);
#6448=AXIS2_PLACEMENT_3D('',#9986,#8252,#8253);
#6449=AXIS2_PLACEMENT_3D('',#9987,#8254,#8255);
#6505=DIRECTION('',(0.,0.,1.));
#6506=DIRECTION('',(1.,0.,0.));
#8192=DIRECTION('',(0.,1.,0.));
#8193=DIRECTION('',(0.,0.,1.));
#8194=DIRECTION('',(0.,1.,0.));
#8195=DIRECTION('',(0.,0.,1.));
#8196=DIRECTION('',(0.,1.,0.));
#8197=DIRECTION('',(0.,0.,1.));
#8198=DIRECTION('',(0.,1.,0.));
#8199=DIRECTION('',(0.,0.,1.));
#8200=DIRECTION('',(0.,1.,0.));
#8201=DIRECTION('',(0.,0.,1.));
#8202=DIRECTION('',(0.,1.,0.));
#8203=DIRECTION('',(0.,0.,1.));
#8204=DIRECTION('',(0.,1.,0.));
#8205=DIRECTION('',(0.,0.,1.));
#8206=DIRECTION('',(0.,1.,0.));
#8207=DIRECTION('',(0.,0.,1.));
#8208=DIRECTION('',(0.,1.,0.));
#8209=DIRECTION('',(0.,0.,1.));
#8210=DIRECTION('',(0.,-1.,0.));
#8211=DIRECTION('',(0.,0.,-1.));
#8212=DIRECTION('',(0.,1.,0.));
#8213=DIRECTION('',(0.,0.,1.));
#8214=DIRECTION('',(0.,1.,0.));
#8215=DIRECTION('',(0.,0.,1.));
#8216=DIRECTION('',(0.,1.,0.));
#8217=DIRECTION('',(0.,0.,1.));
#8218=DIRECTION('',(0.,-1.,0.));
#8219=DIRECTION('',(0.,0.,-1.));
#8220=DIRECTION('',(0.,1.,0.));
#8221=DIRECTION('',(0.,0.,1.));
#8222=DIRECTION('',(0.,1.,0.));
#8223=DIRECTION('',(0.,0.,1.));
#8224=DIRECTION('',(0.,1.,0.));
#8225=DIRECTION('',(0.,0.,1.));
#8226=DIRECTION('',(0.,1.,0.));
#8227=DIRECTION('',(0.,0.,1.));
#8228=DIRECTION('',(0.,1.,0.));
#8229=DIRECTION('',(0.,0.,1.));
#8230=DIRECTION('',(0.,1.,0.));
#8231=DIRECTION('',(0.,0.,1.));
#8232=DIRECTION('',(0.,-1.,0.));
#8233=DIRECTION('',(0.,0.,-1.));
#8234=DIRECTION('',(0.,1.,0.));
#8235=DIRECTION('',(0.,0.,1.));
#8236=DIRECTION('',(0.,1.,0.));
#8237=DIRECTION('',(0.,0.,1.));
#8238=DIRECTION('',(0.,-1.,0.));
#8239=DIRECTION('',(0.,0.,-1.));
#8240=DIRECTION('',(0.,1.,0.));
#8241=DIRECTION('',(0.,0.,1.));
#8242=DIRECTION('',(0.,1.,0.));
#8243=DIRECTION('',(0.,0.,1.));
#8244=DIRECTION('',(0.,-1.,0.));
#8245=DIRECTION('',(0.,0.,-1.));
#8246=DIRECTION('',(0.,1.,0.));
#8247=DIRECTION('',(0.,0.,1.));
#8248=DIRECTION('',(0.,-1.,0.));
#8249=DIRECTION('',(0.,0.,-1.));
#8250=DIRECTION('',(0.,-1.,0.));
#8251=DIRECTION('',(0.,0.,-1.));
#8252=DIRECTION('',(0.,1.,0.));
#8253=DIRECTION('',(0.,0.,1.));
#8254=DIRECTION('',(0.,-1.,0.));
#8255=DIRECTION('',(0.,0.,-1.));
#8391=CARTESIAN_POINT('',(0.,0.,0.));
#9940=CARTESIAN_POINT('',(0.,0.0660090909090909,0.));
#9941=CARTESIAN_POINT('',(0.,0.0396535295792868,0.));
#9942=CARTESIAN_POINT('',(0.,0.0396535295792868,0.0635));
#9943=CARTESIAN_POINT('',(0.,0.0421535295792868,0.));
#9944=CARTESIAN_POINT('',(0.,0.0421535295792868,0.0635));
#9945=CARTESIAN_POINT('',(0.06,0.0421535295792868,0.));
#9946=CARTESIAN_POINT('',(0.,0.0421535295792868,0.));
#9947=CARTESIAN_POINT('',(0.,0.0421535295792868,0.06));
#9948=CARTESIAN_POINT('',(0.,0.0660090909090909,0.));
#9949=CARTESIAN_POINT('',(0.,0.0426535295792868,0.));
#9950=CARTESIAN_POINT('',(0.,0.0426535295792868,0.06));
#9951=CARTESIAN_POINT('',(0.,0.0434387048123469,0.));
#9952=CARTESIAN_POINT('',(0.,0.0434387048123469,0.));
#9953=CARTESIAN_POINT('',(0.,0.0434387048123469,0.0619081467766146));
#9954=CARTESIAN_POINT('',(0.,0.0431535295792868,0.));
#9955=CARTESIAN_POINT('',(0.,0.043251523679028,0.));
#9956=CARTESIAN_POINT('',(0.,0.043251523679028,0.0636093675261996));
#9957=CARTESIAN_POINT('',(0.,0.0660090909090909,0.));
#9958=CARTESIAN_POINT('',(0.,0.0396535295792868,0.));
#9959=CARTESIAN_POINT('',(0.,0.0396535295792868,0.0645));
#9960=CARTESIAN_POINT('',(0.,0.0422575222986401,0.));
#9961=CARTESIAN_POINT('',(0.,0.0422575222986401,-0.0645));
#9962=CARTESIAN_POINT('',(0.0619081467766146,0.0364304487369043,0.));
#9963=CARTESIAN_POINT('',(0.,0.0364304487369043,0.));
#9964=CARTESIAN_POINT('',(0.,0.0364304487369043,0.0629081467766146));
#9965=CARTESIAN_POINT('',(0.,0.0364304487369043,0.));
#9966=CARTESIAN_POINT('',(0.,0.0364304487369043,0.0644389218390369));
#9967=CARTESIAN_POINT('',(0.,0.0660090909090909,0.));
#9968=CARTESIAN_POINT('',(0.,0.0374304487369043,0.));
#9969=CARTESIAN_POINT('',(0.,0.0374304487369043,0.0619081467766146));
#9970=CARTESIAN_POINT('',(0.,0.0396535295792868,0.));
#9971=CARTESIAN_POINT('',(0.,0.0396535295792868,0.0619081467766146));
#9972=CARTESIAN_POINT('',(0.0635,0.0396535295792868,0.));
#9973=CARTESIAN_POINT('',(0.,0.0396535295792868,0.));
#9974=CARTESIAN_POINT('',(0.,0.0386745739867052,0.));
#9975=CARTESIAN_POINT('',(0.,0.0386745739867052,0.0637040733883139));
#9976=CARTESIAN_POINT('',(0.,0.0422575222986401,0.));
#9977=CARTESIAN_POINT('',(0.,0.0376956183941869,0.));
#9978=CARTESIAN_POINT('',(0.,0.0376956183941869,0.));
#9979=CARTESIAN_POINT('',(0.,0.0376956183941869,0.0629081467766146));
#9980=CARTESIAN_POINT('',(0.,0.0384304487369043,0.));
#9981=CARTESIAN_POINT('',(0.,0.0374313822435482,0.));
#9982=CARTESIAN_POINT('',(0.,0.0374313822435482,0.0635431988692856));
#9983=CARTESIAN_POINT('',(0.,0.0364323157506478,0.));
#9984=CARTESIAN_POINT('',(0.,0.0364323157506478,0.));
#9985=CARTESIAN_POINT('',(0.,0.0364323157506478,-0.0645));
#9986=CARTESIAN_POINT('',(0.,0.0374304487369043,0.));
#9987=CARTESIAN_POINT('',(0.,0.0374304487369043,0.));
#10141=MECHANICAL_DESIGN_GEOMETRIC_PRESENTATION_REPRESENTATION('',(#5564),#10142);
#10142=(
GEOMETRIC_REPRESENTATION_CONTEXT(3)
GLOBAL_UNCERTAINTY_ASSIGNED_CONTEXT((#10158))
GLOBAL_UNIT_ASSIGNED_CONTEXT((#10176,#10175,#10174))
REPRESENTATION_CONTEXT('MAS-674','TOP_LEVEL_ASSEMBLY_PART')
);
#10155=(
GEOMETRIC_REPRESENTATION_CONTEXT(3)
GLOBAL_UNCERTAINTY_ASSIGNED_CONTEXT((#10171))
GLOBAL_UNIT_ASSIGNED_CONTEXT((#10176,#10175,#10174))
REPRESENTATION_CONTEXT('Part 1','COMPONENT_PART')
);
#10158=UNCERTAINTY_MEASURE_WITH_UNIT(LENGTH_MEASURE(1.E-8),#10176,
'DISTANCE_ACCURACY_VALUE','Maximum Tolerance applied to model');
#10171=UNCERTAINTY_MEASURE_WITH_UNIT(LENGTH_MEASURE(1.E-8),#10176,
'DISTANCE_ACCURACY_VALUE','Maximum Tolerance applied to model');
#10174=(
NAMED_UNIT(*)
SI_UNIT($,.STERADIAN.)
SOLID_ANGLE_UNIT()
);
#10175=(
NAMED_UNIT(*)
PLANE_ANGLE_UNIT()
SI_UNIT($,.RADIAN.)
);
#10176=(
LENGTH_UNIT()
NAMED_UNIT(*)
SI_UNIT($,.METRE.)
);
#10204=PRODUCT_DEFINITION_SHAPE('','',#10223);
#10223=PRODUCT_DEFINITION('','',#10255,#10239);
#10239=PRODUCT_DEFINITION_CONTEXT('',#10323,'design');
#10255=PRODUCT_DEFINITION_FORMATION_WITH_SPECIFIED_SOURCE('','',#10287,
 .NOT_KNOWN.);
#10287=PRODUCT('Part 1','Part 1','Part 1',(#10319));
#10319=PRODUCT_CONTEXT('',#10323,'mechanical');
#10323=APPLICATION_CONTEXT('managed model based 3d engineering');
ENDSEC;
END-ISO-10303-21;
